ISO-10303-21;
HEADER;
/* Generated by software containing ST-Developer
 * from STEP Tools, Inc. (www.steptools.com) 
 */

FILE_DESCRIPTION(
/* description */ ('PAT-091'),
/* implementation_level */ '2;1');

FILE_NAME(
/* name */ 'Plain pivot bush (1).step',
/* time_stamp */ '2026-10-27T15:34:44-07:00',
/* author */ (''),
/* organization */ (''),
/* preprocessor_version */ 'ST-DEVELOPER v20.2',
/* originating_system */ 'Autodesk Translation Framework v15.17.0.0',
/* authorisation */ '');

FILE_SCHEMA (('AUTOMOTIVE_DESIGN { 1 0 10303 214 3 1 1 }'));
ENDSEC;

DATA;
#10=MECHANICAL_DESIGN_GEOMETRIC_PRESENTATION_REPRESENTATION('',(#1029),#25100);
#809=SHAPE_REPRESENTATION_RELATIONSHIP('SRR','None',#25575,#919);
#919=ADVANCED_BREP_SHAPE_REPRESENTATION('',(#1151),#25045);
#1029=STYLED_ITEM('',(#26177),#1151);
#1151=MANIFOLD_SOLID_BREP('Body1',#13308);
#1492=FACE_BOUND('',#3626,.T.);
#1493=FACE_BOUND('',#3628,.T.);
#1903=PLANE('',#15530);
#1904=PLANE('',#15531);
#2528=FACE_OUTER_BOUND('',#3623,.T.);
#2529=FACE_OUTER_BOUND('',#3624,.T.);
#2530=FACE_OUTER_BOUND('',#3625,.T.);
#2531=FACE_OUTER_BOUND('',#3627,.T.);
#3623=EDGE_LOOP('',(#10852,#10853,#10854,#10855));
#3624=EDGE_LOOP('',(#10856,#10857,#10858,#10859));
#3625=EDGE_LOOP('',(#10860));
#3626=EDGE_LOOP('',(#10861));
#3627=EDGE_LOOP('',(#10862));
#3628=EDGE_LOOP('',(#10863));
#4654=LINE('',#23127,#5394);
#4655=LINE('',#23133,#5395);
#5394=VECTOR('',#18880,0.604999999999997);
#5395=VECTOR('',#18887,1.);
#6010=CIRCLE('',#15525,0.604999999999997);
#6011=CIRCLE('',#15526,0.604999999999997);
#6012=CIRCLE('',#15528,1.);
#6013=CIRCLE('',#15529,1.);
#7007=VERTEX_POINT('',#23124);
#7008=VERTEX_POINT('',#23126);
#7009=VERTEX_POINT('',#23130);
#7010=VERTEX_POINT('',#23132);
#8361=EDGE_CURVE('',#7007,#7007,#6010,.T.);
#8362=EDGE_CURVE('',#7007,#7008,#4654,.T.);
#8363=EDGE_CURVE('',#7008,#7008,#6011,.T.);
#8364=EDGE_CURVE('',#7009,#7009,#6012,.T.);
#8365=EDGE_CURVE('',#7009,#7010,#4655,.T.);
#8366=EDGE_CURVE('',#7010,#7010,#6013,.T.);
#10852=ORIENTED_EDGE('',*,*,#8361,.F.);
#10853=ORIENTED_EDGE('',*,*,#8362,.T.);
#10854=ORIENTED_EDGE('',*,*,#8363,.T.);
#10855=ORIENTED_EDGE('',*,*,#8362,.F.);
#10856=ORIENTED_EDGE('',*,*,#8364,.F.);
#10857=ORIENTED_EDGE('',*,*,#8365,.T.);
#10858=ORIENTED_EDGE('',*,*,#8366,.T.);
#10859=ORIENTED_EDGE('',*,*,#8365,.F.);
#10860=ORIENTED_EDGE('',*,*,#8364,.T.);
#10861=ORIENTED_EDGE('',*,*,#8361,.T.);
#10862=ORIENTED_EDGE('',*,*,#8366,.F.);
#10863=ORIENTED_EDGE('',*,*,#8363,.F.);
#12268=CYLINDRICAL_SURFACE('',#15524,0.604999999999997);
#12269=CYLINDRICAL_SURFACE('',#15527,1.);
#12895=ADVANCED_FACE('',(#2528),#12268,.F.);
#12896=ADVANCED_FACE('',(#2529),#12269,.T.);
#12897=ADVANCED_FACE('',(#2530,#1492),#1903,.T.);
#12898=ADVANCED_FACE('',(#2531,#1493),#1904,.F.);
#13308=CLOSED_SHELL('',(#12895,#12896,#12897,#12898));
#15523=AXIS2_PLACEMENT_3D('',#23122,#18874,#18875);
#15524=AXIS2_PLACEMENT_3D('',#23123,#18876,#18877);
#15525=AXIS2_PLACEMENT_3D('',#23125,#18878,#18879);
#15526=AXIS2_PLACEMENT_3D('',#23128,#18881,#18882);
#15527=AXIS2_PLACEMENT_3D('',#23129,#18883,#18884);
#15528=AXIS2_PLACEMENT_3D('',#23131,#18885,#18886);
#15529=AXIS2_PLACEMENT_3D('',#23134,#18888,#18889);
#15530=AXIS2_PLACEMENT_3D('',#23135,#18890,#18891);
#15531=AXIS2_PLACEMENT_3D('',#23136,#18892,#18893);
#18874=DIRECTION('axis',(0.,0.,1.));
#18875=DIRECTION('refdir',(1.,0.,0.));
#18876=DIRECTION('center_axis',(0.,1.,0.));
#18877=DIRECTION('ref_axis',(1.,0.,0.));
#18878=DIRECTION('center_axis',(0.,-1.,0.));
#18879=DIRECTION('ref_axis',(1.,0.,0.));
#18880=DIRECTION('',(0.,-1.,0.));
#18881=DIRECTION('center_axis',(0.,-1.,0.));
#18882=DIRECTION('ref_axis',(1.,0.,0.));
#18883=DIRECTION('center_axis',(0.,1.,0.));
#18884=DIRECTION('ref_axis',(1.,0.,0.));
#18885=DIRECTION('center_axis',(0.,1.,0.));
#18886=DIRECTION('ref_axis',(1.,0.,0.));
#18887=DIRECTION('',(0.,-1.,0.));
#18888=DIRECTION('center_axis',(0.,1.,0.));
#18889=DIRECTION('ref_axis',(1.,0.,0.));
#18890=DIRECTION('center_axis',(0.,1.,0.));
#18891=DIRECTION('ref_axis',(1.,0.,0.));
#18892=DIRECTION('center_axis',(0.,1.,0.));
#18893=DIRECTION('ref_axis',(1.,0.,0.));
#23122=CARTESIAN_POINT('',(0.,0.,0.));
#23123=CARTESIAN_POINT('Origin',(38.7298334620742,-7.,13.));
#23124=CARTESIAN_POINT('',(38.1248334620742,-6.,13.));
#23125=CARTESIAN_POINT('Origin',(38.7298334620742,-6.,13.));
#23126=CARTESIAN_POINT('',(38.1248334620742,-7.,13.));
#23127=CARTESIAN_POINT('',(38.1248334620742,-7.,13.));
#23128=CARTESIAN_POINT('Origin',(38.7298334620742,-7.,13.));
#23129=CARTESIAN_POINT('Origin',(38.7298334620742,-7.,13.));
#23130=CARTESIAN_POINT('',(37.7298334620742,-6.,13.));
#23131=CARTESIAN_POINT('Origin',(38.7298334620742,-6.,13.));
#23132=CARTESIAN_POINT('',(37.7298334620742,-7.,13.));
#23133=CARTESIAN_POINT('',(37.7298334620742,-7.,13.));
#23134=CARTESIAN_POINT('Origin',(38.7298334620742,-7.,13.));
#23135=CARTESIAN_POINT('Origin',(38.7298334620742,-6.,13.));
#23136=CARTESIAN_POINT('Origin',(38.7298334620742,-7.,13.));
#24924=UNCERTAINTY_MEASURE_WITH_UNIT(LENGTH_MEASURE(0.001),#25101,
'DISTANCE_ACCURACY_VALUE',
'Maximum model space distance between geometric entities at asserted c
onnectivities');
#24979=UNCERTAINTY_MEASURE_WITH_UNIT(LENGTH_MEASURE(0.001),#25101,
'DISTANCE_ACCURACY_VALUE',
'Maximum model space distance between geometric entities at asserted c
onnectivities');
#25045=(
GEOMETRIC_REPRESENTATION_CONTEXT(3)
GLOBAL_UNCERTAINTY_ASSIGNED_CONTEXT((#24924))
GLOBAL_UNIT_ASSIGNED_CONTEXT((#25101,#25103,#25104))
REPRESENTATION_CONTEXT('','3D')
);
#25100=(
GEOMETRIC_REPRESENTATION_CONTEXT(3)
GLOBAL_UNCERTAINTY_ASSIGNED_CONTEXT((#24979))
GLOBAL_UNIT_ASSIGNED_CONTEXT((#25101,#25103,#25104))
REPRESENTATION_CONTEXT('','3D')
);
#25101=(
LENGTH_UNIT()
NAMED_UNIT(*)
SI_UNIT(.CENTI.,.METRE.)
);
#25103=(
NAMED_UNIT(*)
PLANE_ANGLE_UNIT()
SI_UNIT($,.RADIAN.)
);
#25104=(
NAMED_UNIT(*)
SI_UNIT($,.STERADIAN.)
SOLID_ANGLE_UNIT()
);
#25170=SHAPE_DEFINITION_REPRESENTATION(#25292,#25575);
#25292=PRODUCT_DEFINITION_SHAPE('',$,#25696);
#25575=SHAPE_REPRESENTATION('',(#15523),#25045);
#25630=PRODUCT_DEFINITION_CONTEXT('part definition',#25992,'design');
#25696=PRODUCT_DEFINITION('Plain pivot bush (1)','Plain pivot bush (1)',#25816,
#25630);
#25816=PRODUCT_DEFINITION_FORMATION('',$,#26059);
#25992=APPLICATION_CONTEXT(
'Core Data for Automotive Mechanical Design Process');
#25993=PRODUCT_CONTEXT('part definition',#25992,'mechanical');
#26059=PRODUCT('Plain pivot bush (1)','Plain pivot bush (1)',
'Plain pivot bush (1)',(#25993));
#26171=COLOUR_RGB('Light Blue',0.38,0.62,0.78);
#26172=FILL_AREA_STYLE_COLOUR('',#26171);
#26173=FILL_AREA_STYLE('',(#26172));
#26174=SURFACE_STYLE_FILL_AREA(#26173);
#26175=SURFACE_SIDE_STYLE('',(#26174));
#26176=SURFACE_STYLE_USAGE(.BOTH.,#26175);
#26177=PRESENTATION_STYLE_ASSIGNMENT((#26176));
ENDSEC;
END-ISO-10303-21;
